ISO-10303-21;
HEADER;
/* Generated by software containing ST-Developer
 * from STEP Tools, Inc. (www.steptools.com) 
 */

FILE_DESCRIPTION(
/* description */ ('Self-centering screw clamp'),
/* implementation_level */ '2;1');

FILE_NAME(
/* name */ 'Screw bearing post.step',
/* time_stamp */ '2026-10-28T03:25:31-07:00',
/* author */ (''),
/* organization */ (''),
/* preprocessor_version */ 'ST-DEVELOPER v20.2',
/* originating_system */ 'Autodesk Translation Framework v15.17.0.0',
/* authorisation */ '');

FILE_SCHEMA (('AUTOMOTIVE_DESIGN { 1 0 10303 214 3 1 1 }'));
ENDSEC;

DATA;
#10=MECHANICAL_DESIGN_GEOMETRIC_PRESENTATION_REPRESENTATION('',(#631),#16799);
#549=SHAPE_REPRESENTATION_RELATIONSHIP('SRR','None',#17022,#590);
#590=ADVANCED_BREP_SHAPE_REPRESENTATION('',(#679),#16760);
#631=STYLED_ITEM('',(#17333),#679);
#679=MANIFOLD_SOLID_BREP('Body1',#9082);
#770=FACE_BOUND('',#1939,.T.);
#771=FACE_BOUND('',#1941,.T.);
#772=FACE_BOUND('',#1946,.T.);
#773=FACE_BOUND('',#1947,.T.);
#774=FACE_BOUND('',#1948,.T.);
#775=FACE_BOUND('',#1949,.T.);
#776=FACE_BOUND('',#1950,.T.);
#777=FACE_BOUND('',#1953,.T.);
#778=FACE_BOUND('',#1954,.T.);
#779=FACE_BOUND('',#1955,.T.);
#780=FACE_BOUND('',#1956,.T.);
#781=FACE_BOUND('',#1957,.T.);
#782=FACE_BOUND('',#1960,.T.);
#783=FACE_BOUND('',#1961,.T.);
#1072=PLANE('',#9802);
#1073=PLANE('',#9803);
#1074=PLANE('',#9804);
#1075=PLANE('',#9805);
#1076=PLANE('',#9806);
#1077=PLANE('',#9807);
#1078=PLANE('',#9808);
#1079=PLANE('',#9809);
#1080=PLANE('',#9810);
#1081=PLANE('',#9811);
#1375=FACE_OUTER_BOUND('',#1931,.T.);
#1376=FACE_OUTER_BOUND('',#1932,.T.);
#1377=FACE_OUTER_BOUND('',#1933,.T.);
#1378=FACE_OUTER_BOUND('',#1934,.T.);
#1379=FACE_OUTER_BOUND('',#1935,.T.);
#1380=FACE_OUTER_BOUND('',#1936,.T.);
#1381=FACE_OUTER_BOUND('',#1937,.T.);
#1382=FACE_OUTER_BOUND('',#1938,.T.);
#1383=FACE_OUTER_BOUND('',#1940,.T.);
#1384=FACE_OUTER_BOUND('',#1942,.T.);
#1385=FACE_OUTER_BOUND('',#1943,.T.);
#1386=FACE_OUTER_BOUND('',#1944,.T.);
#1387=FACE_OUTER_BOUND('',#1945,.T.);
#1388=FACE_OUTER_BOUND('',#1951,.T.);
#1389=FACE_OUTER_BOUND('',#1952,.T.);
#1390=FACE_OUTER_BOUND('',#1958,.T.);
#1391=FACE_OUTER_BOUND('',#1959,.T.);
#1931=EDGE_LOOP('',(#6631,#6632,#6633,#6634));
#1932=EDGE_LOOP('',(#6635,#6636,#6637,#6638));
#1933=EDGE_LOOP('',(#6639,#6640,#6641,#6642));
#1934=EDGE_LOOP('',(#6643,#6644,#6645,#6646));
#1935=EDGE_LOOP('',(#6647,#6648,#6649,#6650));
#1936=EDGE_LOOP('',(#6651,#6652,#6653,#6654));
#1937=EDGE_LOOP('',(#6655,#6656,#6657,#6658));
#1938=EDGE_LOOP('',(#6659,#6660,#6661,#6662));
#1939=EDGE_LOOP('',(#6663));
#1940=EDGE_LOOP('',(#6664,#6665,#6666,#6667));
#1941=EDGE_LOOP('',(#6668));
#1942=EDGE_LOOP('',(#6669,#6670,#6671,#6672));
#1943=EDGE_LOOP('',(#6673,#6674,#6675,#6676));
#1944=EDGE_LOOP('',(#6677,#6678,#6679,#6680));
#1945=EDGE_LOOP('',(#6681,#6682,#6683,#6684,#6685,#6686,#6687,#6688));
#1946=EDGE_LOOP('',(#6689));
#1947=EDGE_LOOP('',(#6690));
#1948=EDGE_LOOP('',(#6691));
#1949=EDGE_LOOP('',(#6692));
#1950=EDGE_LOOP('',(#6693));
#1951=EDGE_LOOP('',(#6694,#6695,#6696,#6697));
#1952=EDGE_LOOP('',(#6698,#6699,#6700,#6701,#6702,#6703,#6704,#6705));
#1953=EDGE_LOOP('',(#6706));
#1954=EDGE_LOOP('',(#6707));
#1955=EDGE_LOOP('',(#6708));
#1956=EDGE_LOOP('',(#6709));
#1957=EDGE_LOOP('',(#6710));
#1958=EDGE_LOOP('',(#6711,#6712,#6713,#6714));
#1959=EDGE_LOOP('',(#6715,#6716,#6717,#6718));
#1960=EDGE_LOOP('',(#6719));
#1961=EDGE_LOOP('',(#6720));
#2733=LINE('',#14299,#3306);
#2734=LINE('',#14305,#3307);
#2735=LINE('',#14311,#3308);
#2736=LINE('',#14317,#3309);
#2737=LINE('',#14323,#3310);
#2738=LINE('',#14329,#3311);
#2739=LINE('',#14335,#3312);
#2740=LINE('',#14340,#3313);
#2741=LINE('',#14342,#3314);
#2742=LINE('',#14344,#3315);
#2743=LINE('',#14345,#3316);
#2744=LINE('',#14349,#3317);
#2745=LINE('',#14351,#3318);
#2746=LINE('',#14353,#3319);
#2747=LINE('',#14354,#3320);
#2748=LINE('',#14357,#3321);
#2749=LINE('',#14359,#3322);
#2750=LINE('',#14360,#3323);
#2751=LINE('',#14363,#3324);
#2752=LINE('',#14365,#3325);
#2753=LINE('',#14366,#3326);
#2754=LINE('',#14369,#3327);
#2755=LINE('',#14371,#3328);
#2756=LINE('',#14372,#3329);
#2757=LINE('',#14375,#3330);
#2758=LINE('',#14376,#3331);
#2759=LINE('',#14377,#3332);
#2760=LINE('',#14380,#3333);
#2761=LINE('',#14381,#3334);
#2762=LINE('',#14383,#3335);
#2763=LINE('',#14384,#3336);
#3306=VECTOR('',#11320,0.165);
#3307=VECTOR('',#11327,0.165);
#3308=VECTOR('',#11334,0.165);
#3309=VECTOR('',#11341,0.165);
#3310=VECTOR('',#11348,0.225);
#3311=VECTOR('',#11355,0.225);
#3312=VECTOR('',#11362,1.6);
#3313=VECTOR('',#11367,1.);
#3314=VECTOR('',#11368,1.);
#3315=VECTOR('',#11369,1.);
#3316=VECTOR('',#11370,1.);
#3317=VECTOR('',#11373,1.);
#3318=VECTOR('',#11374,1.);
#3319=VECTOR('',#11375,1.);
#3320=VECTOR('',#11376,1.);
#3321=VECTOR('',#11379,1.);
#3322=VECTOR('',#11380,1.);
#3323=VECTOR('',#11381,1.);
#3324=VECTOR('',#11384,1.);
#3325=VECTOR('',#11385,1.);
#3326=VECTOR('',#11386,1.);
#3327=VECTOR('',#11389,1.);
#3328=VECTOR('',#11390,1.);
#3329=VECTOR('',#11391,1.);
#3330=VECTOR('',#11394,1.);
#3331=VECTOR('',#11395,1.);
#3332=VECTOR('',#11396,1.);
#3333=VECTOR('',#11399,1.);
#3334=VECTOR('',#11400,1.);
#3335=VECTOR('',#11403,1.);
#3336=VECTOR('',#11404,1.);
#3815=CIRCLE('',#9782,0.165);
#3816=CIRCLE('',#9783,0.165);
#3817=CIRCLE('',#9785,0.165);
#3818=CIRCLE('',#9786,0.165);
#3819=CIRCLE('',#9788,0.165);
#3820=CIRCLE('',#9789,0.165);
#3821=CIRCLE('',#9791,0.165);
#3822=CIRCLE('',#9792,0.165);
#3823=CIRCLE('',#9794,0.225);
#3824=CIRCLE('',#9795,0.225);
#3825=CIRCLE('',#9797,0.225);
#3826=CIRCLE('',#9798,0.225);
#3827=CIRCLE('',#9800,1.6);
#3828=CIRCLE('',#9801,1.6);
#4397=VERTEX_POINT('',#14296);
#4398=VERTEX_POINT('',#14298);
#4399=VERTEX_POINT('',#14302);
#4400=VERTEX_POINT('',#14304);
#4401=VERTEX_POINT('',#14308);
#4402=VERTEX_POINT('',#14310);
#4403=VERTEX_POINT('',#14314);
#4404=VERTEX_POINT('',#14316);
#4405=VERTEX_POINT('',#14320);
#4406=VERTEX_POINT('',#14322);
#4407=VERTEX_POINT('',#14326);
#4408=VERTEX_POINT('',#14328);
#4409=VERTEX_POINT('',#14332);
#4410=VERTEX_POINT('',#14334);
#4411=VERTEX_POINT('',#14338);
#4412=VERTEX_POINT('',#14339);
#4413=VERTEX_POINT('',#14341);
#4414=VERTEX_POINT('',#14343);
#4415=VERTEX_POINT('',#14347);
#4416=VERTEX_POINT('',#14348);
#4417=VERTEX_POINT('',#14350);
#4418=VERTEX_POINT('',#14352);
#4419=VERTEX_POINT('',#14356);
#4420=VERTEX_POINT('',#14358);
#4421=VERTEX_POINT('',#14362);
#4422=VERTEX_POINT('',#14364);
#4423=VERTEX_POINT('',#14368);
#4424=VERTEX_POINT('',#14370);
#4425=VERTEX_POINT('',#14374);
#4426=VERTEX_POINT('',#14379);
#5240=EDGE_CURVE('',#4397,#4397,#3815,.T.);
#5241=EDGE_CURVE('',#4397,#4398,#2733,.T.);
#5242=EDGE_CURVE('',#4398,#4398,#3816,.T.);
#5243=EDGE_CURVE('',#4399,#4399,#3817,.T.);
#5244=EDGE_CURVE('',#4399,#4400,#2734,.T.);
#5245=EDGE_CURVE('',#4400,#4400,#3818,.T.);
#5246=EDGE_CURVE('',#4401,#4401,#3819,.T.);
#5247=EDGE_CURVE('',#4401,#4402,#2735,.T.);
#5248=EDGE_CURVE('',#4402,#4402,#3820,.T.);
#5249=EDGE_CURVE('',#4403,#4403,#3821,.T.);
#5250=EDGE_CURVE('',#4403,#4404,#2736,.T.);
#5251=EDGE_CURVE('',#4404,#4404,#3822,.T.);
#5252=EDGE_CURVE('',#4405,#4405,#3823,.T.);
#5253=EDGE_CURVE('',#4405,#4406,#2737,.T.);
#5254=EDGE_CURVE('',#4406,#4406,#3824,.T.);
#5255=EDGE_CURVE('',#4407,#4407,#3825,.T.);
#5256=EDGE_CURVE('',#4407,#4408,#2738,.T.);
#5257=EDGE_CURVE('',#4408,#4408,#3826,.T.);
#5258=EDGE_CURVE('',#4409,#4409,#3827,.T.);
#5259=EDGE_CURVE('',#4409,#4410,#2739,.T.);
#5260=EDGE_CURVE('',#4410,#4410,#3828,.T.);
#5261=EDGE_CURVE('',#4411,#4412,#2740,.T.);
#5262=EDGE_CURVE('',#4413,#4411,#2741,.T.);
#5263=EDGE_CURVE('',#4414,#4413,#2742,.T.);
#5264=EDGE_CURVE('',#4414,#4412,#2743,.T.);
#5265=EDGE_CURVE('',#4415,#4416,#2744,.T.);
#5266=EDGE_CURVE('',#4415,#4417,#2745,.T.);
#5267=EDGE_CURVE('',#4417,#4418,#2746,.T.);
#5268=EDGE_CURVE('',#4416,#4418,#2747,.T.);
#5269=EDGE_CURVE('',#4419,#4414,#2748,.T.);
#5270=EDGE_CURVE('',#4420,#4413,#2749,.T.);
#5271=EDGE_CURVE('',#4419,#4420,#2750,.T.);
#5272=EDGE_CURVE('',#4417,#4421,#2751,.T.);
#5273=EDGE_CURVE('',#4421,#4422,#2752,.T.);
#5274=EDGE_CURVE('',#4418,#4422,#2753,.T.);
#5275=EDGE_CURVE('',#4416,#4423,#2754,.T.);
#5276=EDGE_CURVE('',#4424,#4423,#2755,.T.);
#5277=EDGE_CURVE('',#4415,#4424,#2756,.T.);
#5278=EDGE_CURVE('',#4411,#4425,#2757,.T.);
#5279=EDGE_CURVE('',#4423,#4425,#2758,.T.);
#5280=EDGE_CURVE('',#4422,#4420,#2759,.T.);
#5281=EDGE_CURVE('',#4412,#4426,#2760,.T.);
#5282=EDGE_CURVE('',#4425,#4426,#2761,.T.);
#5283=EDGE_CURVE('',#4426,#4424,#2762,.T.);
#5284=EDGE_CURVE('',#4419,#4421,#2763,.T.);
#6631=ORIENTED_EDGE('',*,*,#5240,.F.);
#6632=ORIENTED_EDGE('',*,*,#5241,.T.);
#6633=ORIENTED_EDGE('',*,*,#5242,.F.);
#6634=ORIENTED_EDGE('',*,*,#5241,.F.);
#6635=ORIENTED_EDGE('',*,*,#5243,.F.);
#6636=ORIENTED_EDGE('',*,*,#5244,.T.);
#6637=ORIENTED_EDGE('',*,*,#5245,.F.);
#6638=ORIENTED_EDGE('',*,*,#5244,.F.);
#6639=ORIENTED_EDGE('',*,*,#5246,.F.);
#6640=ORIENTED_EDGE('',*,*,#5247,.T.);
#6641=ORIENTED_EDGE('',*,*,#5248,.F.);
#6642=ORIENTED_EDGE('',*,*,#5247,.F.);
#6643=ORIENTED_EDGE('',*,*,#5249,.F.);
#6644=ORIENTED_EDGE('',*,*,#5250,.T.);
#6645=ORIENTED_EDGE('',*,*,#5251,.F.);
#6646=ORIENTED_EDGE('',*,*,#5250,.F.);
#6647=ORIENTED_EDGE('',*,*,#5252,.F.);
#6648=ORIENTED_EDGE('',*,*,#5253,.T.);
#6649=ORIENTED_EDGE('',*,*,#5254,.F.);
#6650=ORIENTED_EDGE('',*,*,#5253,.F.);
#6651=ORIENTED_EDGE('',*,*,#5255,.F.);
#6652=ORIENTED_EDGE('',*,*,#5256,.T.);
#6653=ORIENTED_EDGE('',*,*,#5257,.F.);
#6654=ORIENTED_EDGE('',*,*,#5256,.F.);
#6655=ORIENTED_EDGE('',*,*,#5258,.F.);
#6656=ORIENTED_EDGE('',*,*,#5259,.T.);
#6657=ORIENTED_EDGE('',*,*,#5260,.F.);
#6658=ORIENTED_EDGE('',*,*,#5259,.F.);
#6659=ORIENTED_EDGE('',*,*,#5261,.F.);
#6660=ORIENTED_EDGE('',*,*,#5262,.F.);
#6661=ORIENTED_EDGE('',*,*,#5263,.F.);
#6662=ORIENTED_EDGE('',*,*,#5264,.T.);
#6663=ORIENTED_EDGE('',*,*,#5257,.T.);
#6664=ORIENTED_EDGE('',*,*,#5265,.F.);
#6665=ORIENTED_EDGE('',*,*,#5266,.T.);
#6666=ORIENTED_EDGE('',*,*,#5267,.T.);
#6667=ORIENTED_EDGE('',*,*,#5268,.F.);
#6668=ORIENTED_EDGE('',*,*,#5254,.T.);
#6669=ORIENTED_EDGE('',*,*,#5269,.T.);
#6670=ORIENTED_EDGE('',*,*,#5263,.T.);
#6671=ORIENTED_EDGE('',*,*,#5270,.F.);
#6672=ORIENTED_EDGE('',*,*,#5271,.F.);
#6673=ORIENTED_EDGE('',*,*,#5272,.T.);
#6674=ORIENTED_EDGE('',*,*,#5273,.T.);
#6675=ORIENTED_EDGE('',*,*,#5274,.F.);
#6676=ORIENTED_EDGE('',*,*,#5267,.F.);
#6677=ORIENTED_EDGE('',*,*,#5265,.T.);
#6678=ORIENTED_EDGE('',*,*,#5275,.T.);
#6679=ORIENTED_EDGE('',*,*,#5276,.F.);
#6680=ORIENTED_EDGE('',*,*,#5277,.F.);
#6681=ORIENTED_EDGE('',*,*,#5278,.T.);
#6682=ORIENTED_EDGE('',*,*,#5279,.F.);
#6683=ORIENTED_EDGE('',*,*,#5275,.F.);
#6684=ORIENTED_EDGE('',*,*,#5268,.T.);
#6685=ORIENTED_EDGE('',*,*,#5274,.T.);
#6686=ORIENTED_EDGE('',*,*,#5280,.T.);
#6687=ORIENTED_EDGE('',*,*,#5270,.T.);
#6688=ORIENTED_EDGE('',*,*,#5262,.T.);
#6689=ORIENTED_EDGE('',*,*,#5260,.T.);
#6690=ORIENTED_EDGE('',*,*,#5251,.T.);
#6691=ORIENTED_EDGE('',*,*,#5248,.T.);
#6692=ORIENTED_EDGE('',*,*,#5245,.T.);
#6693=ORIENTED_EDGE('',*,*,#5242,.T.);
#6694=ORIENTED_EDGE('',*,*,#5261,.T.);
#6695=ORIENTED_EDGE('',*,*,#5281,.T.);
#6696=ORIENTED_EDGE('',*,*,#5282,.F.);
#6697=ORIENTED_EDGE('',*,*,#5278,.F.);
#6698=ORIENTED_EDGE('',*,*,#5277,.T.);
#6699=ORIENTED_EDGE('',*,*,#5283,.F.);
#6700=ORIENTED_EDGE('',*,*,#5281,.F.);
#6701=ORIENTED_EDGE('',*,*,#5264,.F.);
#6702=ORIENTED_EDGE('',*,*,#5269,.F.);
#6703=ORIENTED_EDGE('',*,*,#5284,.T.);
#6704=ORIENTED_EDGE('',*,*,#5272,.F.);
#6705=ORIENTED_EDGE('',*,*,#5266,.F.);
#6706=ORIENTED_EDGE('',*,*,#5258,.T.);
#6707=ORIENTED_EDGE('',*,*,#5249,.T.);
#6708=ORIENTED_EDGE('',*,*,#5246,.T.);
#6709=ORIENTED_EDGE('',*,*,#5243,.T.);
#6710=ORIENTED_EDGE('',*,*,#5240,.T.);
#6711=ORIENTED_EDGE('',*,*,#5283,.T.);
#6712=ORIENTED_EDGE('',*,*,#5276,.T.);
#6713=ORIENTED_EDGE('',*,*,#5279,.T.);
#6714=ORIENTED_EDGE('',*,*,#5282,.T.);
#6715=ORIENTED_EDGE('',*,*,#5284,.F.);
#6716=ORIENTED_EDGE('',*,*,#5271,.T.);
#6717=ORIENTED_EDGE('',*,*,#5280,.F.);
#6718=ORIENTED_EDGE('',*,*,#5273,.F.);
#6719=ORIENTED_EDGE('',*,*,#5252,.T.);
#6720=ORIENTED_EDGE('',*,*,#5255,.T.);
#8401=CYLINDRICAL_SURFACE('',#9781,0.165);
#8402=CYLINDRICAL_SURFACE('',#9784,0.165);
#8403=CYLINDRICAL_SURFACE('',#9787,0.165);
#8404=CYLINDRICAL_SURFACE('',#9790,0.165);
#8405=CYLINDRICAL_SURFACE('',#9793,0.225);
#8406=CYLINDRICAL_SURFACE('',#9796,0.225);
#8407=CYLINDRICAL_SURFACE('',#9799,1.6);
#8673=ADVANCED_FACE('',(#1375),#8401,.F.);
#8674=ADVANCED_FACE('',(#1376),#8402,.F.);
#8675=ADVANCED_FACE('',(#1377),#8403,.F.);
#8676=ADVANCED_FACE('',(#1378),#8404,.F.);
#8677=ADVANCED_FACE('',(#1379),#8405,.F.);
#8678=ADVANCED_FACE('',(#1380),#8406,.F.);
#8679=ADVANCED_FACE('',(#1381),#8407,.F.);
#8680=ADVANCED_FACE('',(#1382,#770),#1072,.T.);
#8681=ADVANCED_FACE('',(#1383,#771),#1073,.T.);
#8682=ADVANCED_FACE('',(#1384),#1074,.T.);
#8683=ADVANCED_FACE('',(#1385),#1075,.T.);
#8684=ADVANCED_FACE('',(#1386),#1076,.T.);
#8685=ADVANCED_FACE('',(#1387,#772,#773,#774,#775,#776),#1077,.T.);
#8686=ADVANCED_FACE('',(#1388),#1078,.T.);
#8687=ADVANCED_FACE('',(#1389,#777,#778,#779,#780,#781),#1079,.T.);
#8688=ADVANCED_FACE('',(#1390),#1080,.T.);
#8689=ADVANCED_FACE('',(#1391,#782,#783),#1081,.F.);
#9082=CLOSED_SHELL('',(#8673,#8674,#8675,#8676,#8677,#8678,#8679,#8680,
#8681,#8682,#8683,#8684,#8685,#8686,#8687,#8688,#8689));
#9780=AXIS2_PLACEMENT_3D('',#14294,#11314,#11315);
#9781=AXIS2_PLACEMENT_3D('',#14295,#11316,#11317);
#9782=AXIS2_PLACEMENT_3D('',#14297,#11318,#11319);
#9783=AXIS2_PLACEMENT_3D('',#14300,#11321,#11322);
#9784=AXIS2_PLACEMENT_3D('',#14301,#11323,#11324);
#9785=AXIS2_PLACEMENT_3D('',#14303,#11325,#11326);
#9786=AXIS2_PLACEMENT_3D('',#14306,#11328,#11329);
#9787=AXIS2_PLACEMENT_3D('',#14307,#11330,#11331);
#9788=AXIS2_PLACEMENT_3D('',#14309,#11332,#11333);
#9789=AXIS2_PLACEMENT_3D('',#14312,#11335,#11336);
#9790=AXIS2_PLACEMENT_3D('',#14313,#11337,#11338);
#9791=AXIS2_PLACEMENT_3D('',#14315,#11339,#11340);
#9792=AXIS2_PLACEMENT_3D('',#14318,#11342,#11343);
#9793=AXIS2_PLACEMENT_3D('',#14319,#11344,#11345);
#9794=AXIS2_PLACEMENT_3D('',#14321,#11346,#11347);
#9795=AXIS2_PLACEMENT_3D('',#14324,#11349,#11350);
#9796=AXIS2_PLACEMENT_3D('',#14325,#11351,#11352);
#9797=AXIS2_PLACEMENT_3D('',#14327,#11353,#11354);
#9798=AXIS2_PLACEMENT_3D('',#14330,#11356,#11357);
#9799=AXIS2_PLACEMENT_3D('',#14331,#11358,#11359);
#9800=AXIS2_PLACEMENT_3D('',#14333,#11360,#11361);
#9801=AXIS2_PLACEMENT_3D('',#14336,#11363,#11364);
#9802=AXIS2_PLACEMENT_3D('',#14337,#11365,#11366);
#9803=AXIS2_PLACEMENT_3D('',#14346,#11371,#11372);
#9804=AXIS2_PLACEMENT_3D('',#14355,#11377,#11378);
#9805=AXIS2_PLACEMENT_3D('',#14361,#11382,#11383);
#9806=AXIS2_PLACEMENT_3D('',#14367,#11387,#11388);
#9807=AXIS2_PLACEMENT_3D('',#14373,#11392,#11393);
#9808=AXIS2_PLACEMENT_3D('',#14378,#11397,#11398);
#9809=AXIS2_PLACEMENT_3D('',#14382,#11401,#11402);
#9810=AXIS2_PLACEMENT_3D('',#14385,#11405,#11406);
#9811=AXIS2_PLACEMENT_3D('',#14386,#11407,#11408);
#11314=DIRECTION('axis',(0.,0.,1.));
#11315=DIRECTION('refdir',(1.,0.,0.));
#11316=DIRECTION('center_axis',(1.,0.,0.));
#11317=DIRECTION('ref_axis',(0.,0.,-1.));
#11318=DIRECTION('center_axis',(1.,0.,0.));
#11319=DIRECTION('ref_axis',(0.,0.,-1.));
#11320=DIRECTION('',(1.,0.,0.));
#11321=DIRECTION('center_axis',(-1.,0.,0.));
#11322=DIRECTION('ref_axis',(0.,0.,-1.));
#11323=DIRECTION('center_axis',(1.,0.,0.));
#11324=DIRECTION('ref_axis',(0.,0.,-1.));
#11325=DIRECTION('center_axis',(1.,0.,0.));
#11326=DIRECTION('ref_axis',(0.,0.,-1.));
#11327=DIRECTION('',(1.,0.,0.));
#11328=DIRECTION('center_axis',(-1.,0.,0.));
#11329=DIRECTION('ref_axis',(0.,0.,-1.));
#11330=DIRECTION('center_axis',(1.,0.,0.));
#11331=DIRECTION('ref_axis',(0.,0.,-1.));
#11332=DIRECTION('center_axis',(1.,0.,0.));
#11333=DIRECTION('ref_axis',(0.,0.,-1.));
#11334=DIRECTION('',(1.,0.,0.));
#11335=DIRECTION('center_axis',(-1.,0.,0.));
#11336=DIRECTION('ref_axis',(0.,0.,-1.));
#11337=DIRECTION('center_axis',(1.,0.,0.));
#11338=DIRECTION('ref_axis',(0.,0.,-1.));
#11339=DIRECTION('center_axis',(1.,0.,0.));
#11340=DIRECTION('ref_axis',(0.,0.,-1.));
#11341=DIRECTION('',(1.,0.,0.));
#11342=DIRECTION('center_axis',(-1.,0.,0.));
#11343=DIRECTION('ref_axis',(0.,0.,-1.));
#11344=DIRECTION('center_axis',(0.,0.,1.));
#11345=DIRECTION('ref_axis',(1.,0.,0.));
#11346=DIRECTION('center_axis',(0.,0.,1.));
#11347=DIRECTION('ref_axis',(1.,0.,0.));
#11348=DIRECTION('',(0.,0.,1.));
#11349=DIRECTION('center_axis',(0.,0.,-1.));
#11350=DIRECTION('ref_axis',(1.,0.,0.));
#11351=DIRECTION('center_axis',(0.,0.,1.));
#11352=DIRECTION('ref_axis',(1.,0.,0.));
#11353=DIRECTION('center_axis',(0.,0.,1.));
#11354=DIRECTION('ref_axis',(1.,0.,0.));
#11355=DIRECTION('',(0.,0.,1.));
#11356=DIRECTION('center_axis',(0.,0.,-1.));
#11357=DIRECTION('ref_axis',(1.,0.,0.));
#11358=DIRECTION('center_axis',(1.,0.,0.));
#11359=DIRECTION('ref_axis',(0.,0.,-1.));
#11360=DIRECTION('center_axis',(1.,0.,0.));
#11361=DIRECTION('ref_axis',(0.,0.,-1.));
#11362=DIRECTION('',(1.,0.,0.));
#11363=DIRECTION('center_axis',(-1.,0.,0.));
#11364=DIRECTION('ref_axis',(0.,0.,-1.));
#11365=DIRECTION('center_axis',(0.,0.,1.));
#11366=DIRECTION('ref_axis',(0.,-1.,0.));
#11367=DIRECTION('',(-1.,0.,0.));
#11368=DIRECTION('',(0.,-1.,0.));
#11369=DIRECTION('',(1.,0.,0.));
#11370=DIRECTION('',(0.,-1.,0.));
#11371=DIRECTION('center_axis',(0.,0.,1.));
#11372=DIRECTION('ref_axis',(0.,-1.,0.));
#11373=DIRECTION('',(1.,0.,0.));
#11374=DIRECTION('',(0.,-1.,0.));
#11375=DIRECTION('',(1.,0.,0.));
#11376=DIRECTION('',(0.,-1.,0.));
#11377=DIRECTION('center_axis',(0.,1.,0.));
#11378=DIRECTION('ref_axis',(0.,0.,1.));
#11379=DIRECTION('',(0.,0.,1.));
#11380=DIRECTION('',(0.,0.,1.));
#11381=DIRECTION('',(1.,0.,0.));
#11382=DIRECTION('center_axis',(0.,-1.,0.));
#11383=DIRECTION('ref_axis',(0.,0.,-1.));
#11384=DIRECTION('',(0.,0.,-1.));
#11385=DIRECTION('',(1.,0.,0.));
#11386=DIRECTION('',(0.,0.,-1.));
#11387=DIRECTION('center_axis',(0.,-1.,0.));
#11388=DIRECTION('ref_axis',(1.,0.,0.));
#11389=DIRECTION('',(0.,0.,1.));
#11390=DIRECTION('',(1.,0.,0.));
#11391=DIRECTION('',(0.,0.,1.));
#11392=DIRECTION('center_axis',(1.,0.,0.));
#11393=DIRECTION('ref_axis',(0.,1.,0.));
#11394=DIRECTION('',(0.,0.,1.));
#11395=DIRECTION('',(0.,1.,0.));
#11396=DIRECTION('',(0.,1.,0.));
#11397=DIRECTION('center_axis',(0.,1.,0.));
#11398=DIRECTION('ref_axis',(-1.,0.,0.));
#11399=DIRECTION('',(0.,0.,1.));
#11400=DIRECTION('',(-1.,0.,0.));
#11401=DIRECTION('center_axis',(-1.,0.,0.));
#11402=DIRECTION('ref_axis',(0.,-1.,0.));
#11403=DIRECTION('',(0.,-1.,0.));
#11404=DIRECTION('',(0.,-1.,0.));
#11405=DIRECTION('center_axis',(0.,0.,1.));
#11406=DIRECTION('ref_axis',(1.,0.,0.));
#11407=DIRECTION('center_axis',(0.,0.,1.));
#11408=DIRECTION('ref_axis',(1.,0.,0.));
#14294=CARTESIAN_POINT('',(0.,0.,0.));
#14295=CARTESIAN_POINT('Origin',(-12.4,-1.4142135623731,2.58578643762691));
#14296=CARTESIAN_POINT('',(-12.3,-1.4142135623731,2.75078643762691));
#14297=CARTESIAN_POINT('Origin',(-12.3,-1.4142135623731,2.58578643762691));
#14298=CARTESIAN_POINT('',(-10.7,-1.4142135623731,2.75078643762691));
#14299=CARTESIAN_POINT('',(-12.4,-1.4142135623731,2.75078643762691));
#14300=CARTESIAN_POINT('Origin',(-10.7,-1.4142135623731,2.58578643762691));
#14301=CARTESIAN_POINT('Origin',(-12.4,-1.41421356237309,5.41421356237309));
#14302=CARTESIAN_POINT('',(-12.3,-1.41421356237309,5.57921356237309));
#14303=CARTESIAN_POINT('Origin',(-12.3,-1.41421356237309,5.41421356237309));
#14304=CARTESIAN_POINT('',(-10.7,-1.41421356237309,5.57921356237309));
#14305=CARTESIAN_POINT('',(-12.4,-1.41421356237309,5.57921356237309));
#14306=CARTESIAN_POINT('Origin',(-10.7,-1.41421356237309,5.41421356237309));
#14307=CARTESIAN_POINT('Origin',(-12.4,1.4142135623731,5.41421356237309));
#14308=CARTESIAN_POINT('',(-12.3,1.4142135623731,5.57921356237309));
#14309=CARTESIAN_POINT('Origin',(-12.3,1.4142135623731,5.41421356237309));
#14310=CARTESIAN_POINT('',(-10.7,1.4142135623731,5.57921356237309));
#14311=CARTESIAN_POINT('',(-12.4,1.4142135623731,5.57921356237309));
#14312=CARTESIAN_POINT('Origin',(-10.7,1.4142135623731,5.41421356237309));
#14313=CARTESIAN_POINT('Origin',(-12.4,1.41421356237309,2.5857864376269));
#14314=CARTESIAN_POINT('',(-12.3,1.41421356237309,2.7507864376269));
#14315=CARTESIAN_POINT('Origin',(-12.3,1.41421356237309,2.5857864376269));
#14316=CARTESIAN_POINT('',(-10.7,1.41421356237309,2.7507864376269));
#14317=CARTESIAN_POINT('',(-12.4,1.41421356237309,2.7507864376269));
#14318=CARTESIAN_POINT('Origin',(-10.7,1.41421356237309,2.5857864376269));
#14319=CARTESIAN_POINT('Origin',(-11.5,-3.,0.9));
#14320=CARTESIAN_POINT('',(-11.725,-3.,1.));
#14321=CARTESIAN_POINT('Origin',(-11.5,-3.,1.));
#14322=CARTESIAN_POINT('',(-11.725,-3.,1.8));
#14323=CARTESIAN_POINT('',(-11.725,-3.,0.9));
#14324=CARTESIAN_POINT('Origin',(-11.5,-3.,1.8));
#14325=CARTESIAN_POINT('Origin',(-11.5,3.,0.9));
#14326=CARTESIAN_POINT('',(-11.725,3.,1.));
#14327=CARTESIAN_POINT('Origin',(-11.5,3.,1.));
#14328=CARTESIAN_POINT('',(-11.725,3.,1.8));
#14329=CARTESIAN_POINT('',(-11.725,3.,0.9));
#14330=CARTESIAN_POINT('Origin',(-11.5,3.,1.8));
#14331=CARTESIAN_POINT('Origin',(-12.4,0.,4.));
#14332=CARTESIAN_POINT('',(-12.3,-1.95943487863577E-16,5.6));
#14333=CARTESIAN_POINT('Origin',(-12.3,0.,4.));
#14334=CARTESIAN_POINT('',(-10.7,1.95943487863577E-16,5.6));
#14335=CARTESIAN_POINT('',(-12.4,-1.95943487863577E-16,5.6));
#14336=CARTESIAN_POINT('Origin',(-10.7,0.,4.));
#14337=CARTESIAN_POINT('Origin',(-12.3,3.6,1.8));
#14338=CARTESIAN_POINT('',(-10.7,2.4,1.8));
#14339=CARTESIAN_POINT('',(-12.3,2.4,1.8));
#14340=CARTESIAN_POINT('',(-11.5,2.4,1.8));
#14341=CARTESIAN_POINT('',(-10.7,3.6,1.8));
#14342=CARTESIAN_POINT('',(-10.7,3.6,1.8));
#14343=CARTESIAN_POINT('',(-12.3,3.6,1.8));
#14344=CARTESIAN_POINT('',(-12.3,3.6,1.8));
#14345=CARTESIAN_POINT('',(-12.3,3.6,1.8));
#14346=CARTESIAN_POINT('Origin',(-12.3,3.6,1.8));
#14347=CARTESIAN_POINT('',(-12.3,-2.4,1.8));
#14348=CARTESIAN_POINT('',(-10.7,-2.4,1.8));
#14349=CARTESIAN_POINT('',(-12.3,-2.4,1.8));
#14350=CARTESIAN_POINT('',(-12.3,-3.6,1.8));
#14351=CARTESIAN_POINT('',(-12.3,3.6,1.8));
#14352=CARTESIAN_POINT('',(-10.7,-3.6,1.8));
#14353=CARTESIAN_POINT('',(-12.3,-3.6,1.8));
#14354=CARTESIAN_POINT('',(-10.7,3.6,1.8));
#14355=CARTESIAN_POINT('Origin',(-12.3,3.6,1.));
#14356=CARTESIAN_POINT('',(-12.3,3.6,1.));
#14357=CARTESIAN_POINT('',(-12.3,3.6,1.));
#14358=CARTESIAN_POINT('',(-10.7,3.6,1.));
#14359=CARTESIAN_POINT('',(-10.7,3.6,1.));
#14360=CARTESIAN_POINT('',(-12.3,3.6,1.));
#14361=CARTESIAN_POINT('Origin',(-12.3,-3.6,1.8));
#14362=CARTESIAN_POINT('',(-12.3,-3.6,1.));
#14363=CARTESIAN_POINT('',(-12.3,-3.6,1.8));
#14364=CARTESIAN_POINT('',(-10.7,-3.6,1.));
#14365=CARTESIAN_POINT('',(-12.3,-3.6,1.));
#14366=CARTESIAN_POINT('',(-10.7,-3.6,1.8));
#14367=CARTESIAN_POINT('Origin',(-12.3,-2.4,1.));
#14368=CARTESIAN_POINT('',(-10.7,-2.4,6.5));
#14369=CARTESIAN_POINT('',(-10.7,-2.4,1.));
#14370=CARTESIAN_POINT('',(-12.3,-2.4,6.5));
#14371=CARTESIAN_POINT('',(-12.3,-2.4,6.5));
#14372=CARTESIAN_POINT('',(-12.3,-2.4,1.));
#14373=CARTESIAN_POINT('Origin',(-10.7,-2.4,1.));
#14374=CARTESIAN_POINT('',(-10.7,2.4,6.5));
#14375=CARTESIAN_POINT('',(-10.7,2.4,1.));
#14376=CARTESIAN_POINT('',(-10.7,-2.4,6.5));
#14377=CARTESIAN_POINT('',(-10.7,-3.6,1.));
#14378=CARTESIAN_POINT('Origin',(-10.7,2.4,1.));
#14379=CARTESIAN_POINT('',(-12.3,2.4,6.5));
#14380=CARTESIAN_POINT('',(-12.3,2.4,1.));
#14381=CARTESIAN_POINT('',(-10.7,2.4,6.5));
#14382=CARTESIAN_POINT('Origin',(-12.3,2.4,1.));
#14383=CARTESIAN_POINT('',(-12.3,2.4,6.5));
#14384=CARTESIAN_POINT('',(-12.3,2.4,1.));
#14385=CARTESIAN_POINT('Origin',(-11.5,0.,6.5));
#14386=CARTESIAN_POINT('Origin',(-11.5,0.,1.));
#16711=UNCERTAINTY_MEASURE_WITH_UNIT(LENGTH_MEASURE(0.001),#16800,
'DISTANCE_ACCURACY_VALUE',
'Maximum model space distance between geometric entities at asserted c
onnectivities');
#16750=UNCERTAINTY_MEASURE_WITH_UNIT(LENGTH_MEASURE(0.001),#16800,
'DISTANCE_ACCURACY_VALUE',
'Maximum model space distance between geometric entities at asserted c
onnectivities');
#16760=(
GEOMETRIC_REPRESENTATION_CONTEXT(3)
GLOBAL_UNCERTAINTY_ASSIGNED_CONTEXT((#16711))
GLOBAL_UNIT_ASSIGNED_CONTEXT((#16800,#16802,#16803))
REPRESENTATION_CONTEXT('','3D')
);
#16799=(
GEOMETRIC_REPRESENTATION_CONTEXT(3)
GLOBAL_UNCERTAINTY_ASSIGNED_CONTEXT((#16750))
GLOBAL_UNIT_ASSIGNED_CONTEXT((#16800,#16802,#16803))
REPRESENTATION_CONTEXT('','3D')
);
#16800=(
LENGTH_UNIT()
NAMED_UNIT(*)
SI_UNIT(.CENTI.,.METRE.)
);
#16802=(
NAMED_UNIT(*)
PLANE_ANGLE_UNIT()
SI_UNIT($,.RADIAN.)
);
#16803=(
NAMED_UNIT(*)
SI_UNIT($,.STERADIAN.)
SOLID_ANGLE_UNIT()
);
#16813=SHAPE_DEFINITION_REPRESENTATION(#16861,#17022);
#16861=PRODUCT_DEFINITION_SHAPE('',$,#17071);
#17022=SHAPE_REPRESENTATION('',(#9780),#16760);
#17061=PRODUCT_DEFINITION_CONTEXT('part definition',#17207,'design');
#17071=PRODUCT_DEFINITION('Screw bearing post','Screw bearing post',#17119,
#17061);
#17119=PRODUCT_DEFINITION_FORMATION('',$,#17218);
#17207=APPLICATION_CONTEXT(
'Core Data for Automotive Mechanical Design Process');
#17208=PRODUCT_CONTEXT('part definition',#17207,'mechanical');
#17218=PRODUCT('Screw bearing post','Screw bearing post',
'Screw bearing post',(#17208));
#17327=COLOUR_RGB('Black',0.12,0.14,0.17);
#17328=FILL_AREA_STYLE_COLOUR('',#17327);
#17329=FILL_AREA_STYLE('',(#17328));
#17330=SURFACE_STYLE_FILL_AREA(#17329);
#17331=SURFACE_SIDE_STYLE('',(#17330));
#17332=SURFACE_STYLE_USAGE(.BOTH.,#17331);
#17333=PRESENTATION_STYLE_ASSIGNMENT((#17332));
ENDSEC;
END-ISO-10303-21;
